ISO-10303-21;
HEADER;
/* Generated by software containing ST-Developer
 * from STEP Tools, Inc. (www.steptools.com) 
 */

FILE_DESCRIPTION(
/* description */ (''),
/* implementation_level */ '2;1');

FILE_NAME(
/* name */ 'Blade_02.step',
/* time_stamp */ '2026-10-23T22:28:14+06:00',
/* author */ (''),
/* organization */ (''),
/* preprocessor_version */ 'ST-DEVELOPER v20.2',
/* originating_system */ 'Autodesk Translation Framework v15.15.0.0',
/* authorisation */ '');

FILE_SCHEMA (('AUTOMOTIVE_DESIGN { 1 0 10303 214 3 1 1 }'));
ENDSEC;

DATA;
#10=MECHANICAL_DESIGN_GEOMETRIC_PRESENTATION_REPRESENTATION('',(#109),#6753);
#83=SHAPE_REPRESENTATION_RELATIONSHIP('SRR','None',#6806,#96);
#96=ADVANCED_BREP_SHAPE_REPRESENTATION('',(#122),#6746);
#109=STYLED_ITEM('',(#6907),#122);
#122=MANIFOLD_SOLID_BREP('Blade_02',#3758);
#172=FACE_BOUND('',#735,.T.);
#173=FACE_BOUND('',#736,.T.);
#291=PLANE('',#4220);
#292=PLANE('',#4221);
#293=PLANE('',#4222);
#294=PLANE('',#4229);
#295=PLANE('',#4232);
#296=PLANE('',#4237);
#476=FACE_OUTER_BOUND('',#732,.T.);
#477=FACE_OUTER_BOUND('',#733,.T.);
#478=FACE_OUTER_BOUND('',#734,.T.);
#479=FACE_OUTER_BOUND('',#737,.T.);
#480=FACE_OUTER_BOUND('',#738,.T.);
#481=FACE_OUTER_BOUND('',#739,.T.);
#482=FACE_OUTER_BOUND('',#740,.T.);
#483=FACE_OUTER_BOUND('',#741,.T.);
#484=FACE_OUTER_BOUND('',#742,.T.);
#485=FACE_OUTER_BOUND('',#743,.T.);
#732=EDGE_LOOP('',(#3226,#3227,#3228,#3229));
#733=EDGE_LOOP('',(#3230,#3231,#3232,#3233));
#734=EDGE_LOOP('',(#3234,#3235,#3236,#3237));
#735=EDGE_LOOP('',(#3238));
#736=EDGE_LOOP('',(#3239));
#737=EDGE_LOOP('',(#3240,#3241,#3242,#3243));
#738=EDGE_LOOP('',(#3244));
#739=EDGE_LOOP('',(#3245,#3246,#3247,#3248));
#740=EDGE_LOOP('',(#3249));
#741=EDGE_LOOP('',(#3250,#3251,#3252,#3253));
#742=EDGE_LOOP('',(#3254,#3255,#3256,#3257));
#743=EDGE_LOOP('',(#3258,#3259,#3260,#3261));
#976=CIRCLE('',#4223,33.8);
#977=CIRCLE('',#4224,4.99999999999999);
#978=CIRCLE('',#4225,1.1);
#979=CIRCLE('',#4226,1.1);
#980=CIRCLE('',#4228,1.1);
#981=CIRCLE('',#4231,1.1);
#982=CIRCLE('',#4234,4.99999999999999);
#983=CIRCLE('',#4236,33.8);
#1248=LINE('',#6428,#1534);
#1249=LINE('',#6430,#1535);
#1250=LINE('',#6432,#1536);
#1251=LINE('',#6433,#1537);
#1252=LINE('',#6437,#1538);
#1253=LINE('',#6439,#1539);
#1254=LINE('',#6441,#1540);
#1255=LINE('',#6442,#1541);
#1256=LINE('',#6453,#1542);
#1257=LINE('',#6458,#1543);
#1534=VECTOR('',#5205,10.);
#1535=VECTOR('',#5206,10.);
#1536=VECTOR('',#5207,10.);
#1537=VECTOR('',#5208,10.);
#1538=VECTOR('',#5211,10.);
#1539=VECTOR('',#5212,10.);
#1540=VECTOR('',#5213,10.);
#1541=VECTOR('',#5214,10.);
#1542=VECTOR('',#5229,1.1);
#1543=VECTOR('',#5236,1.1);
#1861=VERTEX_POINT('',#6426);
#1862=VERTEX_POINT('',#6427);
#1863=VERTEX_POINT('',#6429);
#1864=VERTEX_POINT('',#6431);
#1865=VERTEX_POINT('',#6435);
#1866=VERTEX_POINT('',#6436);
#1867=VERTEX_POINT('',#6438);
#1868=VERTEX_POINT('',#6440);
#1869=VERTEX_POINT('',#6446);
#1870=VERTEX_POINT('',#6448);
#1871=VERTEX_POINT('',#6451);
#1872=VERTEX_POINT('',#6456);
#2330=EDGE_CURVE('',#1861,#1862,#1248,.T.);
#2331=EDGE_CURVE('',#1863,#1861,#1249,.T.);
#2332=EDGE_CURVE('',#1864,#1863,#1250,.T.);
#2333=EDGE_CURVE('',#1862,#1864,#1251,.T.);
#2334=EDGE_CURVE('',#1865,#1866,#1252,.T.);
#2335=EDGE_CURVE('',#1867,#1865,#1253,.T.);
#2336=EDGE_CURVE('',#1868,#1867,#1254,.T.);
#2337=EDGE_CURVE('',#1866,#1868,#1255,.T.);
#2338=EDGE_CURVE('',#1865,#1862,#976,.T.);
#2339=EDGE_CURVE('',#1861,#1866,#977,.T.);
#2340=EDGE_CURVE('',#1869,#1869,#978,.T.);
#2341=EDGE_CURVE('',#1870,#1870,#979,.T.);
#2342=EDGE_CURVE('',#1871,#1871,#980,.T.);
#2343=EDGE_CURVE('',#1871,#1869,#1256,.T.);
#2344=EDGE_CURVE('',#1872,#1872,#981,.T.);
#2345=EDGE_CURVE('',#1872,#1870,#1257,.T.);
#2346=EDGE_CURVE('',#1863,#1868,#982,.T.);
#2347=EDGE_CURVE('',#1867,#1864,#983,.T.);
#3226=ORIENTED_EDGE('',*,*,#2330,.F.);
#3227=ORIENTED_EDGE('',*,*,#2331,.F.);
#3228=ORIENTED_EDGE('',*,*,#2332,.F.);
#3229=ORIENTED_EDGE('',*,*,#2333,.F.);
#3230=ORIENTED_EDGE('',*,*,#2334,.F.);
#3231=ORIENTED_EDGE('',*,*,#2335,.F.);
#3232=ORIENTED_EDGE('',*,*,#2336,.F.);
#3233=ORIENTED_EDGE('',*,*,#2337,.F.);
#3234=ORIENTED_EDGE('',*,*,#2330,.T.);
#3235=ORIENTED_EDGE('',*,*,#2338,.F.);
#3236=ORIENTED_EDGE('',*,*,#2334,.T.);
#3237=ORIENTED_EDGE('',*,*,#2339,.F.);
#3238=ORIENTED_EDGE('',*,*,#2340,.T.);
#3239=ORIENTED_EDGE('',*,*,#2341,.T.);
#3240=ORIENTED_EDGE('',*,*,#2342,.F.);
#3241=ORIENTED_EDGE('',*,*,#2343,.T.);
#3242=ORIENTED_EDGE('',*,*,#2340,.F.);
#3243=ORIENTED_EDGE('',*,*,#2343,.F.);
#3244=ORIENTED_EDGE('',*,*,#2342,.T.);
#3245=ORIENTED_EDGE('',*,*,#2344,.F.);
#3246=ORIENTED_EDGE('',*,*,#2345,.T.);
#3247=ORIENTED_EDGE('',*,*,#2341,.F.);
#3248=ORIENTED_EDGE('',*,*,#2345,.F.);
#3249=ORIENTED_EDGE('',*,*,#2344,.T.);
#3250=ORIENTED_EDGE('',*,*,#2331,.T.);
#3251=ORIENTED_EDGE('',*,*,#2339,.T.);
#3252=ORIENTED_EDGE('',*,*,#2337,.T.);
#3253=ORIENTED_EDGE('',*,*,#2346,.F.);
#3254=ORIENTED_EDGE('',*,*,#2333,.T.);
#3255=ORIENTED_EDGE('',*,*,#2347,.F.);
#3256=ORIENTED_EDGE('',*,*,#2335,.T.);
#3257=ORIENTED_EDGE('',*,*,#2338,.T.);
#3258=ORIENTED_EDGE('',*,*,#2332,.T.);
#3259=ORIENTED_EDGE('',*,*,#2346,.T.);
#3260=ORIENTED_EDGE('',*,*,#2336,.T.);
#3261=ORIENTED_EDGE('',*,*,#2347,.T.);
#3511=CYLINDRICAL_SURFACE('',#4227,1.1);
#3512=CYLINDRICAL_SURFACE('',#4230,1.1);
#3513=CYLINDRICAL_SURFACE('',#4233,4.99999999999999);
#3514=CYLINDRICAL_SURFACE('',#4235,33.8);
#3682=ADVANCED_FACE('',(#476),#291,.F.);
#3683=ADVANCED_FACE('',(#477),#292,.F.);
#3684=ADVANCED_FACE('',(#478,#172,#173),#293,.F.);
#3685=ADVANCED_FACE('',(#479),#3511,.T.);
#3686=ADVANCED_FACE('',(#480),#294,.F.);
#3687=ADVANCED_FACE('',(#481),#3512,.T.);
#3688=ADVANCED_FACE('',(#482),#295,.F.);
#3689=ADVANCED_FACE('',(#483),#3513,.F.);
#3690=ADVANCED_FACE('',(#484),#3514,.T.);
#3691=ADVANCED_FACE('',(#485),#296,.T.);
#3758=CLOSED_SHELL('',(#3682,#3683,#3684,#3685,#3686,#3687,#3688,#3689,
#3690,#3691));
#4219=AXIS2_PLACEMENT_3D('',#6424,#5201,#5202);
#4220=AXIS2_PLACEMENT_3D('',#6425,#5203,#5204);
#4221=AXIS2_PLACEMENT_3D('',#6434,#5209,#5210);
#4222=AXIS2_PLACEMENT_3D('',#6443,#5215,#5216);
#4223=AXIS2_PLACEMENT_3D('',#6444,#5217,#5218);
#4224=AXIS2_PLACEMENT_3D('',#6445,#5219,#5220);
#4225=AXIS2_PLACEMENT_3D('',#6447,#5221,#5222);
#4226=AXIS2_PLACEMENT_3D('',#6449,#5223,#5224);
#4227=AXIS2_PLACEMENT_3D('',#6450,#5225,#5226);
#4228=AXIS2_PLACEMENT_3D('',#6452,#5227,#5228);
#4229=AXIS2_PLACEMENT_3D('',#6454,#5230,#5231);
#4230=AXIS2_PLACEMENT_3D('',#6455,#5232,#5233);
#4231=AXIS2_PLACEMENT_3D('',#6457,#5234,#5235);
#4232=AXIS2_PLACEMENT_3D('',#6459,#5237,#5238);
#4233=AXIS2_PLACEMENT_3D('',#6460,#5239,#5240);
#4234=AXIS2_PLACEMENT_3D('',#6461,#5241,#5242);
#4235=AXIS2_PLACEMENT_3D('',#6462,#5243,#5244);
#4236=AXIS2_PLACEMENT_3D('',#6463,#5245,#5246);
#4237=AXIS2_PLACEMENT_3D('',#6464,#5247,#5248);
#5201=DIRECTION('axis',(0.,0.,1.));
#5202=DIRECTION('refdir',(1.,0.,0.));
#5203=DIRECTION('center_axis',(-1.,0.,1.11022302462516E-16));
#5204=DIRECTION('ref_axis',(1.11022302462516E-16,0.,1.));
#5205=DIRECTION('',(1.11022302462516E-16,0.,1.));
#5206=DIRECTION('',(0.,-1.,0.));
#5207=DIRECTION('',(-1.11022302462516E-16,0.,-1.));
#5208=DIRECTION('',(0.,1.,0.));
#5209=DIRECTION('center_axis',(0.707106781186548,0.,0.707106781186548));
#5210=DIRECTION('ref_axis',(0.707106781186548,0.,-0.707106781186548));
#5211=DIRECTION('',(0.707106781186548,0.,-0.707106781186548));
#5212=DIRECTION('',(0.,-1.,0.));
#5213=DIRECTION('',(-0.707106781186548,0.,0.707106781186548));
#5214=DIRECTION('',(0.,1.,0.));
#5215=DIRECTION('center_axis',(0.,1.,0.));
#5216=DIRECTION('ref_axis',(0.707106781186548,0.,0.707106781186548));
#5217=DIRECTION('center_axis',(0.,1.,0.));
#5218=DIRECTION('ref_axis',(0.707106781186547,0.,0.707106781186547));
#5219=DIRECTION('center_axis',(0.,-1.,0.));
#5220=DIRECTION('ref_axis',(0.707106781186548,0.,0.707106781186548));
#5221=DIRECTION('center_axis',(0.,1.,0.));
#5222=DIRECTION('ref_axis',(0.707106781186547,0.,0.707106781186547));
#5223=DIRECTION('center_axis',(0.,1.,0.));
#5224=DIRECTION('ref_axis',(0.707106781186548,0.,0.707106781186548));
#5225=DIRECTION('center_axis',(0.,-1.,0.));
#5226=DIRECTION('ref_axis',(0.707106781186547,0.,0.707106781186547));
#5227=DIRECTION('center_axis',(0.,-1.,0.));
#5228=DIRECTION('ref_axis',(0.707106781186547,0.,0.707106781186547));
#5229=DIRECTION('',(0.,1.,0.));
#5230=DIRECTION('center_axis',(0.,1.,0.));
#5231=DIRECTION('ref_axis',(0.707106781186548,0.,0.707106781186548));
#5232=DIRECTION('center_axis',(0.,-1.,0.));
#5233=DIRECTION('ref_axis',(0.707106781186548,0.,0.707106781186548));
#5234=DIRECTION('center_axis',(0.,-1.,0.));
#5235=DIRECTION('ref_axis',(0.707106781186548,0.,0.707106781186548));
#5236=DIRECTION('',(0.,1.,0.));
#5237=DIRECTION('center_axis',(0.,1.,0.));
#5238=DIRECTION('ref_axis',(0.707106781186548,0.,0.707106781186548));
#5239=DIRECTION('center_axis',(0.,1.,0.));
#5240=DIRECTION('ref_axis',(0.707106781186548,0.,0.707106781186548));
#5241=DIRECTION('center_axis',(0.,-1.,0.));
#5242=DIRECTION('ref_axis',(0.707106781186548,0.,0.707106781186548));
#5243=DIRECTION('center_axis',(0.,1.,0.));
#5244=DIRECTION('ref_axis',(0.707106781186547,0.,0.707106781186547));
#5245=DIRECTION('center_axis',(0.,1.,0.));
#5246=DIRECTION('ref_axis',(0.707106781186547,0.,0.707106781186547));
#5247=DIRECTION('center_axis',(0.,1.,0.));
#5248=DIRECTION('ref_axis',(0.707106781186548,0.,0.707106781186548));
#6424=CARTESIAN_POINT('',(0.,0.,0.));
#6425=CARTESIAN_POINT('Origin',(0.,-3.,119.33240815703));
#6426=CARTESIAN_POINT('',(0.,-3.,119.33240815703));
#6427=CARTESIAN_POINT('',(0.,-3.,148.13240815703));
#6428=CARTESIAN_POINT('',(0.,-3.,116.83240815703));
#6429=CARTESIAN_POINT('',(0.,-2.9,119.33240815703));
#6430=CARTESIAN_POINT('',(0.,-3.,119.33240815703));
#6431=CARTESIAN_POINT('',(0.,-2.9,148.13240815703));
#6432=CARTESIAN_POINT('',(0.,-2.9,116.83240815703));
#6433=CARTESIAN_POINT('',(0.,-3.,148.13240815703));
#6434=CARTESIAN_POINT('Origin',(-23.9002092041053,-3.,138.232617361136));
#6435=CARTESIAN_POINT('',(-23.9002092041053,-3.,138.232617361136));
#6436=CARTESIAN_POINT('',(-3.53553390593273,-3.,117.867942062963));
#6437=CARTESIAN_POINT('',(-11.9501046020527,-3.,126.282512759083));
#6438=CARTESIAN_POINT('',(-23.9002092041053,-2.9,138.232617361136));
#6439=CARTESIAN_POINT('',(-23.9002092041053,-3.,138.232617361136));
#6440=CARTESIAN_POINT('',(-3.53553390593273,-2.9,117.867942062963));
#6441=CARTESIAN_POINT('',(-11.9501046020527,-2.9,126.282512759083));
#6442=CARTESIAN_POINT('',(-3.53553390593273,-3.,117.867942062963));
#6443=CARTESIAN_POINT('Origin',(0.,-3.,114.33240815703));
#6444=CARTESIAN_POINT('Origin',(0.,-3.,114.33240815703));
#6445=CARTESIAN_POINT('Origin',(0.,-3.,114.33240815703));
#6446=CARTESIAN_POINT('',(-16.5043001764605,-3.,138.196865826448));
#6447=CARTESIAN_POINT('Origin',(-15.7264827171553,-3.,138.974683285753));
#6448=CARTESIAN_POINT('',(-5.87700253253308,-3.,142.339348708895));
#6449=CARTESIAN_POINT('Origin',(-5.09918507322789,-3.,143.1171661682));
#6450=CARTESIAN_POINT('Origin',(-15.7264827171553,-3.,138.974683285753));
#6451=CARTESIAN_POINT('',(-16.5043001764605,-3.5,138.196865826448));
#6452=CARTESIAN_POINT('Origin',(-15.7264827171553,-3.5,138.974683285753));
#6453=CARTESIAN_POINT('',(-16.5043001764605,-3.,138.196865826448));
#6454=CARTESIAN_POINT('Origin',(-15.7264827171553,-3.5,138.974683285753));
#6455=CARTESIAN_POINT('Origin',(-5.09918507322789,-3.,143.1171661682));
#6456=CARTESIAN_POINT('',(-5.87700253253308,-3.5,142.339348708895));
#6457=CARTESIAN_POINT('Origin',(-5.09918507322789,-3.5,143.1171661682));
#6458=CARTESIAN_POINT('',(-5.87700253253309,-3.,142.339348708895));
#6459=CARTESIAN_POINT('Origin',(-5.09918507322789,-3.5,143.1171661682));
#6460=CARTESIAN_POINT('Origin',(0.,-3.,114.33240815703));
#6461=CARTESIAN_POINT('Origin',(0.,-2.9,114.33240815703));
#6462=CARTESIAN_POINT('Origin',(0.,-3.,114.33240815703));
#6463=CARTESIAN_POINT('Origin',(0.,-2.9,114.33240815703));
#6464=CARTESIAN_POINT('Origin',(0.,-2.9,114.33240815703));
#6731=UNCERTAINTY_MEASURE_WITH_UNIT(LENGTH_MEASURE(0.01),#6754,
'DISTANCE_ACCURACY_VALUE',
'Maximum model space distance between geometric entities at asserted c
onnectivities');
#6738=UNCERTAINTY_MEASURE_WITH_UNIT(LENGTH_MEASURE(0.01),#6754,
'DISTANCE_ACCURACY_VALUE',
'Maximum model space distance between geometric entities at asserted c
onnectivities');
#6746=(
GEOMETRIC_REPRESENTATION_CONTEXT(3)
GLOBAL_UNCERTAINTY_ASSIGNED_CONTEXT((#6731))
GLOBAL_UNIT_ASSIGNED_CONTEXT((#6754,#6756,#6757))
REPRESENTATION_CONTEXT('','3D')
);
#6753=(
GEOMETRIC_REPRESENTATION_CONTEXT(3)
GLOBAL_UNCERTAINTY_ASSIGNED_CONTEXT((#6738))
GLOBAL_UNIT_ASSIGNED_CONTEXT((#6754,#6756,#6757))
REPRESENTATION_CONTEXT('','3D')
);
#6754=(
LENGTH_UNIT()
NAMED_UNIT(*)
SI_UNIT(.MILLI.,.METRE.)
);
#6756=(
NAMED_UNIT(*)
PLANE_ANGLE_UNIT()
SI_UNIT($,.RADIAN.)
);
#6757=(
NAMED_UNIT(*)
SI_UNIT($,.STERADIAN.)
SOLID_ANGLE_UNIT()
);
#6765=SHAPE_DEFINITION_REPRESENTATION(#6779,#6806);
#6779=PRODUCT_DEFINITION_SHAPE('',$,#6821);
#6806=SHAPE_REPRESENTATION('',(#4219),#6746);
#6813=PRODUCT_DEFINITION_CONTEXT('part definition',#6857,'design');
#6821=PRODUCT_DEFINITION('Blade_02','Blade_02',#6835,#6813);
#6835=PRODUCT_DEFINITION_FORMATION('',$,#6866);
#6857=APPLICATION_CONTEXT(
'Core Data for Automotive Mechanical Design Process');
#6858=PRODUCT_CONTEXT('part definition',#6857,'mechanical');
#6866=PRODUCT('Blade_02','Blade_02',$,(#6858));
#6901=COLOUR_RGB('Light Blue',0.38,0.62,0.78);
#6902=FILL_AREA_STYLE_COLOUR('',#6901);
#6903=FILL_AREA_STYLE('',(#6902));
#6904=SURFACE_STYLE_FILL_AREA(#6903);
#6905=SURFACE_SIDE_STYLE('',(#6904));
#6906=SURFACE_STYLE_USAGE(.BOTH.,#6905);
#6907=PRESENTATION_STYLE_ASSIGNMENT((#6906));
ENDSEC;
END-ISO-10303-21;
